ISO-10303-21;
HEADER;
/* Generated by software containing ST-Developer
 * from STEP Tools, Inc. (www.steptools.com) 
 */

FILE_DESCRIPTION(
/* description */ ('STEP AP214'),
/* implementation_level */ '2;1');

FILE_NAME(
/* name */ 'Ball Screw Support Spacer.step',
/* time_stamp */ '2026-11-15T14:55:55-08:00',
/* author */ (''),
/* organization */ (''),
/* preprocessor_version */ 'ST-DEVELOPER v20.2',
/* originating_system */ 'Autodesk Translation Framework v15.17.0.0',
/* authorisation */ '');

FILE_SCHEMA (('AUTOMOTIVE_DESIGN { 1 0 10303 214 3 1 1 }'));
ENDSEC;

DATA;
#10=MECHANICAL_DESIGN_GEOMETRIC_PRESENTATION_REPRESENTATION('',(#946),#57079);
#886=SHAPE_REPRESENTATION_RELATIONSHIP('SRR','None',#57275,#915);
#915=ADVANCED_BREP_SHAPE_REPRESENTATION('',(#983),#57067);
#946=STYLED_ITEM('',(#57444),#983);
#983=MANIFOLD_SOLID_BREP('Body1',#24546);
#1183=FACE_BOUND('',#4383,.T.);
#1184=FACE_BOUND('',#4384,.T.);
#1185=FACE_BOUND('',#4385,.T.);
#1186=FACE_BOUND('',#4386,.T.);
#1187=FACE_BOUND('',#4387,.T.);
#1188=FACE_BOUND('',#4388,.T.);
#1189=FACE_BOUND('',#4390,.T.);
#1190=FACE_BOUND('',#4391,.T.);
#1191=FACE_BOUND('',#4392,.T.);
#1192=FACE_BOUND('',#4393,.T.);
#1193=FACE_BOUND('',#4394,.T.);
#1194=FACE_BOUND('',#4395,.T.);
#1674=PLANE('',#26062);
#1675=PLANE('',#26063);
#1676=PLANE('',#26064);
#1677=PLANE('',#26065);
#1678=PLANE('',#26066);
#1679=PLANE('',#26067);
#2814=FACE_OUTER_BOUND('',#4372,.T.);
#2815=FACE_OUTER_BOUND('',#4373,.T.);
#2816=FACE_OUTER_BOUND('',#4374,.T.);
#2817=FACE_OUTER_BOUND('',#4375,.T.);
#2818=FACE_OUTER_BOUND('',#4376,.T.);
#2819=FACE_OUTER_BOUND('',#4377,.T.);
#2820=FACE_OUTER_BOUND('',#4378,.T.);
#2821=FACE_OUTER_BOUND('',#4379,.T.);
#2822=FACE_OUTER_BOUND('',#4380,.T.);
#2823=FACE_OUTER_BOUND('',#4381,.T.);
#2824=FACE_OUTER_BOUND('',#4382,.T.);
#2825=FACE_OUTER_BOUND('',#4389,.T.);
#4372=EDGE_LOOP('',(#19012,#19013,#19014,#19015));
#4373=EDGE_LOOP('',(#19016,#19017,#19018,#19019));
#4374=EDGE_LOOP('',(#19020,#19021,#19022,#19023));
#4375=EDGE_LOOP('',(#19024,#19025,#19026,#19027));
#4376=EDGE_LOOP('',(#19028,#19029,#19030,#19031));
#4377=EDGE_LOOP('',(#19032,#19033,#19034,#19035));
#4378=EDGE_LOOP('',(#19036,#19037,#19038,#19039));
#4379=EDGE_LOOP('',(#19040,#19041,#19042,#19043));
#4380=EDGE_LOOP('',(#19044,#19045,#19046,#19047));
#4381=EDGE_LOOP('',(#19048,#19049,#19050,#19051));
#4382=EDGE_LOOP('',(#19052,#19053,#19054,#19055));
#4383=EDGE_LOOP('',(#19056));
#4384=EDGE_LOOP('',(#19057));
#4385=EDGE_LOOP('',(#19058));
#4386=EDGE_LOOP('',(#19059));
#4387=EDGE_LOOP('',(#19060));
#4388=EDGE_LOOP('',(#19061));
#4389=EDGE_LOOP('',(#19062,#19063,#19064,#19065));
#4390=EDGE_LOOP('',(#19066));
#4391=EDGE_LOOP('',(#19067));
#4392=EDGE_LOOP('',(#19068));
#4393=EDGE_LOOP('',(#19069));
#4394=EDGE_LOOP('',(#19070));
#4395=EDGE_LOOP('',(#19071));
#6017=LINE('',#52929,#7984);
#6018=LINE('',#52935,#7985);
#6019=LINE('',#52941,#7986);
#6020=LINE('',#52947,#7987);
#6021=LINE('',#52953,#7988);
#6022=LINE('',#52959,#7989);
#6023=LINE('',#52964,#7990);
#6024=LINE('',#52966,#7991);
#6025=LINE('',#52968,#7992);
#6026=LINE('',#52969,#7993);
#6027=LINE('',#52972,#7994);
#6028=LINE('',#52974,#7995);
#6029=LINE('',#52975,#7996);
#6030=LINE('',#52978,#7997);
#6031=LINE('',#52980,#7998);
#6032=LINE('',#52981,#7999);
#6033=LINE('',#52983,#8000);
#6034=LINE('',#52984,#8001);
#7984=VECTOR('',#30569,3.3);
#7985=VECTOR('',#30576,3.3);
#7986=VECTOR('',#30583,3.3);
#7987=VECTOR('',#30590,3.3);
#7988=VECTOR('',#30597,3.3);
#7989=VECTOR('',#30604,3.3);
#7990=VECTOR('',#30609,1000.);
#7991=VECTOR('',#30610,1000.);
#7992=VECTOR('',#30611,1000.);
#7993=VECTOR('',#30612,1000.);
#7994=VECTOR('',#30615,1000.);
#7995=VECTOR('',#30616,1000.);
#7996=VECTOR('',#30617,1000.);
#7997=VECTOR('',#30620,1000.);
#7998=VECTOR('',#30621,1000.);
#7999=VECTOR('',#30622,1000.);
#8000=VECTOR('',#30625,1000.);
#8001=VECTOR('',#30626,1000.);
#9696=CIRCLE('',#26045,3.3);
#9697=CIRCLE('',#26046,3.3);
#9698=CIRCLE('',#26048,3.3);
#9699=CIRCLE('',#26049,3.3);
#9700=CIRCLE('',#26051,3.3);
#9701=CIRCLE('',#26052,3.3);
#9702=CIRCLE('',#26054,3.3);
#9703=CIRCLE('',#26055,3.3);
#9704=CIRCLE('',#26057,3.3);
#9705=CIRCLE('',#26058,3.3);
#9706=CIRCLE('',#26060,3.3);
#9707=CIRCLE('',#26061,3.3);
#11269=VERTEX_POINT('',#52926);
#11270=VERTEX_POINT('',#52928);
#11271=VERTEX_POINT('',#52932);
#11272=VERTEX_POINT('',#52934);
#11273=VERTEX_POINT('',#52938);
#11274=VERTEX_POINT('',#52940);
#11275=VERTEX_POINT('',#52944);
#11276=VERTEX_POINT('',#52946);
#11277=VERTEX_POINT('',#52950);
#11278=VERTEX_POINT('',#52952);
#11279=VERTEX_POINT('',#52956);
#11280=VERTEX_POINT('',#52958);
#11281=VERTEX_POINT('',#52962);
#11282=VERTEX_POINT('',#52963);
#11283=VERTEX_POINT('',#52965);
#11284=VERTEX_POINT('',#52967);
#11285=VERTEX_POINT('',#52971);
#11286=VERTEX_POINT('',#52973);
#11287=VERTEX_POINT('',#52977);
#11288=VERTEX_POINT('',#52979);
#14051=EDGE_CURVE('',#11269,#11269,#9696,.T.);
#14052=EDGE_CURVE('',#11269,#11270,#6017,.T.);
#14053=EDGE_CURVE('',#11270,#11270,#9697,.T.);
#14054=EDGE_CURVE('',#11271,#11271,#9698,.T.);
#14055=EDGE_CURVE('',#11271,#11272,#6018,.T.);
#14056=EDGE_CURVE('',#11272,#11272,#9699,.T.);
#14057=EDGE_CURVE('',#11273,#11273,#9700,.T.);
#14058=EDGE_CURVE('',#11273,#11274,#6019,.T.);
#14059=EDGE_CURVE('',#11274,#11274,#9701,.T.);
#14060=EDGE_CURVE('',#11275,#11275,#9702,.T.);
#14061=EDGE_CURVE('',#11275,#11276,#6020,.T.);
#14062=EDGE_CURVE('',#11276,#11276,#9703,.T.);
#14063=EDGE_CURVE('',#11277,#11277,#9704,.T.);
#14064=EDGE_CURVE('',#11277,#11278,#6021,.T.);
#14065=EDGE_CURVE('',#11278,#11278,#9705,.T.);
#14066=EDGE_CURVE('',#11279,#11279,#9706,.T.);
#14067=EDGE_CURVE('',#11279,#11280,#6022,.T.);
#14068=EDGE_CURVE('',#11280,#11280,#9707,.T.);
#14069=EDGE_CURVE('',#11281,#11282,#6023,.T.);
#14070=EDGE_CURVE('',#11283,#11282,#6024,.T.);
#14071=EDGE_CURVE('',#11284,#11283,#6025,.T.);
#14072=EDGE_CURVE('',#11284,#11281,#6026,.T.);
#14073=EDGE_CURVE('',#11282,#11285,#6027,.T.);
#14074=EDGE_CURVE('',#11286,#11285,#6028,.T.);
#14075=EDGE_CURVE('',#11283,#11286,#6029,.T.);
#14076=EDGE_CURVE('',#11285,#11287,#6030,.T.);
#14077=EDGE_CURVE('',#11288,#11287,#6031,.T.);
#14078=EDGE_CURVE('',#11286,#11288,#6032,.T.);
#14079=EDGE_CURVE('',#11287,#11281,#6033,.T.);
#14080=EDGE_CURVE('',#11288,#11284,#6034,.T.);
#19012=ORIENTED_EDGE('',*,*,#14051,.F.);
#19013=ORIENTED_EDGE('',*,*,#14052,.T.);
#19014=ORIENTED_EDGE('',*,*,#14053,.T.);
#19015=ORIENTED_EDGE('',*,*,#14052,.F.);
#19016=ORIENTED_EDGE('',*,*,#14054,.F.);
#19017=ORIENTED_EDGE('',*,*,#14055,.T.);
#19018=ORIENTED_EDGE('',*,*,#14056,.T.);
#19019=ORIENTED_EDGE('',*,*,#14055,.F.);
#19020=ORIENTED_EDGE('',*,*,#14057,.F.);
#19021=ORIENTED_EDGE('',*,*,#14058,.T.);
#19022=ORIENTED_EDGE('',*,*,#14059,.T.);
#19023=ORIENTED_EDGE('',*,*,#14058,.F.);
#19024=ORIENTED_EDGE('',*,*,#14060,.F.);
#19025=ORIENTED_EDGE('',*,*,#14061,.T.);
#19026=ORIENTED_EDGE('',*,*,#14062,.T.);
#19027=ORIENTED_EDGE('',*,*,#14061,.F.);
#19028=ORIENTED_EDGE('',*,*,#14063,.F.);
#19029=ORIENTED_EDGE('',*,*,#14064,.T.);
#19030=ORIENTED_EDGE('',*,*,#14065,.T.);
#19031=ORIENTED_EDGE('',*,*,#14064,.F.);
#19032=ORIENTED_EDGE('',*,*,#14066,.F.);
#19033=ORIENTED_EDGE('',*,*,#14067,.T.);
#19034=ORIENTED_EDGE('',*,*,#14068,.T.);
#19035=ORIENTED_EDGE('',*,*,#14067,.F.);
#19036=ORIENTED_EDGE('',*,*,#14069,.T.);
#19037=ORIENTED_EDGE('',*,*,#14070,.F.);
#19038=ORIENTED_EDGE('',*,*,#14071,.F.);
#19039=ORIENTED_EDGE('',*,*,#14072,.T.);
#19040=ORIENTED_EDGE('',*,*,#14073,.T.);
#19041=ORIENTED_EDGE('',*,*,#14074,.F.);
#19042=ORIENTED_EDGE('',*,*,#14075,.F.);
#19043=ORIENTED_EDGE('',*,*,#14070,.T.);
#19044=ORIENTED_EDGE('',*,*,#14076,.T.);
#19045=ORIENTED_EDGE('',*,*,#14077,.F.);
#19046=ORIENTED_EDGE('',*,*,#14078,.F.);
#19047=ORIENTED_EDGE('',*,*,#14074,.T.);
#19048=ORIENTED_EDGE('',*,*,#14079,.T.);
#19049=ORIENTED_EDGE('',*,*,#14072,.F.);
#19050=ORIENTED_EDGE('',*,*,#14080,.F.);
#19051=ORIENTED_EDGE('',*,*,#14077,.T.);
#19052=ORIENTED_EDGE('',*,*,#14071,.T.);
#19053=ORIENTED_EDGE('',*,*,#14075,.T.);
#19054=ORIENTED_EDGE('',*,*,#14078,.T.);
#19055=ORIENTED_EDGE('',*,*,#14080,.T.);
#19056=ORIENTED_EDGE('',*,*,#14053,.F.);
#19057=ORIENTED_EDGE('',*,*,#14056,.F.);
#19058=ORIENTED_EDGE('',*,*,#14059,.F.);
#19059=ORIENTED_EDGE('',*,*,#14062,.F.);
#19060=ORIENTED_EDGE('',*,*,#14065,.F.);
#19061=ORIENTED_EDGE('',*,*,#14068,.F.);
#19062=ORIENTED_EDGE('',*,*,#14069,.F.);
#19063=ORIENTED_EDGE('',*,*,#14079,.F.);
#19064=ORIENTED_EDGE('',*,*,#14076,.F.);
#19065=ORIENTED_EDGE('',*,*,#14073,.F.);
#19066=ORIENTED_EDGE('',*,*,#14051,.T.);
#19067=ORIENTED_EDGE('',*,*,#14054,.T.);
#19068=ORIENTED_EDGE('',*,*,#14057,.T.);
#19069=ORIENTED_EDGE('',*,*,#14060,.T.);
#19070=ORIENTED_EDGE('',*,*,#14063,.T.);
#19071=ORIENTED_EDGE('',*,*,#14066,.T.);
#22902=CYLINDRICAL_SURFACE('',#26044,3.3);
#22903=CYLINDRICAL_SURFACE('',#26047,3.3);
#22904=CYLINDRICAL_SURFACE('',#26050,3.3);
#22905=CYLINDRICAL_SURFACE('',#26053,3.3);
#22906=CYLINDRICAL_SURFACE('',#26056,3.3);
#22907=CYLINDRICAL_SURFACE('',#26059,3.3);
#23806=ADVANCED_FACE('',(#2814),#22902,.F.);
#23807=ADVANCED_FACE('',(#2815),#22903,.F.);
#23808=ADVANCED_FACE('',(#2816),#22904,.F.);
#23809=ADVANCED_FACE('',(#2817),#22905,.F.);
#23810=ADVANCED_FACE('',(#2818),#22906,.F.);
#23811=ADVANCED_FACE('',(#2819),#22907,.F.);
#23812=ADVANCED_FACE('',(#2820),#1674,.F.);
#23813=ADVANCED_FACE('',(#2821),#1675,.F.);
#23814=ADVANCED_FACE('',(#2822),#1676,.F.);
#23815=ADVANCED_FACE('',(#2823),#1677,.F.);
#23816=ADVANCED_FACE('',(#2824,#1183,#1184,#1185,#1186,#1187,#1188),#1678,
 .T.);
#23817=ADVANCED_FACE('',(#2825,#1189,#1190,#1191,#1192,#1193,#1194),#1679,
 .F.);
#24546=CLOSED_SHELL('',(#23806,#23807,#23808,#23809,#23810,#23811,#23812,
#23813,#23814,#23815,#23816,#23817));
#26043=AXIS2_PLACEMENT_3D('',#52924,#30563,#30564);
#26044=AXIS2_PLACEMENT_3D('',#52925,#30565,#30566);
#26045=AXIS2_PLACEMENT_3D('',#52927,#30567,#30568);
#26046=AXIS2_PLACEMENT_3D('',#52930,#30570,#30571);
#26047=AXIS2_PLACEMENT_3D('',#52931,#30572,#30573);
#26048=AXIS2_PLACEMENT_3D('',#52933,#30574,#30575);
#26049=AXIS2_PLACEMENT_3D('',#52936,#30577,#30578);
#26050=AXIS2_PLACEMENT_3D('',#52937,#30579,#30580);
#26051=AXIS2_PLACEMENT_3D('',#52939,#30581,#30582);
#26052=AXIS2_PLACEMENT_3D('',#52942,#30584,#30585);
#26053=AXIS2_PLACEMENT_3D('',#52943,#30586,#30587);
#26054=AXIS2_PLACEMENT_3D('',#52945,#30588,#30589);
#26055=AXIS2_PLACEMENT_3D('',#52948,#30591,#30592);
#26056=AXIS2_PLACEMENT_3D('',#52949,#30593,#30594);
#26057=AXIS2_PLACEMENT_3D('',#52951,#30595,#30596);
#26058=AXIS2_PLACEMENT_3D('',#52954,#30598,#30599);
#26059=AXIS2_PLACEMENT_3D('',#52955,#30600,#30601);
#26060=AXIS2_PLACEMENT_3D('',#52957,#30602,#30603);
#26061=AXIS2_PLACEMENT_3D('',#52960,#30605,#30606);
#26062=AXIS2_PLACEMENT_3D('',#52961,#30607,#30608);
#26063=AXIS2_PLACEMENT_3D('',#52970,#30613,#30614);
#26064=AXIS2_PLACEMENT_3D('',#52976,#30618,#30619);
#26065=AXIS2_PLACEMENT_3D('',#52982,#30623,#30624);
#26066=AXIS2_PLACEMENT_3D('',#52985,#30627,#30628);
#26067=AXIS2_PLACEMENT_3D('',#52986,#30629,#30630);
#30563=DIRECTION('axis',(0.,0.,1.));
#30564=DIRECTION('refdir',(1.,0.,0.));
#30565=DIRECTION('center_axis',(0.,0.,1.));
#30566=DIRECTION('ref_axis',(1.,0.,0.));
#30567=DIRECTION('center_axis',(0.,0.,1.));
#30568=DIRECTION('ref_axis',(1.,0.,0.));
#30569=DIRECTION('',(0.,0.,1.));
#30570=DIRECTION('center_axis',(0.,0.,1.));
#30571=DIRECTION('ref_axis',(1.,0.,0.));
#30572=DIRECTION('center_axis',(0.,0.,1.));
#30573=DIRECTION('ref_axis',(1.,0.,0.));
#30574=DIRECTION('center_axis',(0.,0.,1.));
#30575=DIRECTION('ref_axis',(1.,0.,0.));
#30576=DIRECTION('',(0.,0.,1.));
#30577=DIRECTION('center_axis',(0.,0.,1.));
#30578=DIRECTION('ref_axis',(1.,0.,0.));
#30579=DIRECTION('center_axis',(0.,0.,1.));
#30580=DIRECTION('ref_axis',(1.,0.,0.));
#30581=DIRECTION('center_axis',(0.,0.,1.));
#30582=DIRECTION('ref_axis',(1.,0.,0.));
#30583=DIRECTION('',(0.,0.,1.));
#30584=DIRECTION('center_axis',(0.,0.,1.));
#30585=DIRECTION('ref_axis',(1.,0.,0.));
#30586=DIRECTION('center_axis',(0.,0.,1.));
#30587=DIRECTION('ref_axis',(1.,0.,0.));
#30588=DIRECTION('center_axis',(0.,0.,1.));
#30589=DIRECTION('ref_axis',(1.,0.,0.));
#30590=DIRECTION('',(0.,0.,1.));
#30591=DIRECTION('center_axis',(0.,0.,1.));
#30592=DIRECTION('ref_axis',(1.,0.,0.));
#30593=DIRECTION('center_axis',(0.,0.,1.));
#30594=DIRECTION('ref_axis',(1.,0.,0.));
#30595=DIRECTION('center_axis',(0.,0.,1.));
#30596=DIRECTION('ref_axis',(1.,0.,0.));
#30597=DIRECTION('',(0.,0.,1.));
#30598=DIRECTION('center_axis',(0.,0.,1.));
#30599=DIRECTION('ref_axis',(1.,0.,0.));
#30600=DIRECTION('center_axis',(0.,0.,1.));
#30601=DIRECTION('ref_axis',(1.,0.,0.));
#30602=DIRECTION('center_axis',(0.,0.,1.));
#30603=DIRECTION('ref_axis',(1.,0.,0.));
#30604=DIRECTION('',(0.,0.,1.));
#30605=DIRECTION('center_axis',(0.,0.,1.));
#30606=DIRECTION('ref_axis',(1.,0.,0.));
#30607=DIRECTION('center_axis',(-1.,-2.77555756156289E-16,0.));
#30608=DIRECTION('ref_axis',(2.77555756156289E-16,-1.,0.));
#30609=DIRECTION('',(-2.77555756156289E-16,1.,0.));
#30610=DIRECTION('',(0.,0.,-1.));
#30611=DIRECTION('',(-2.77555756156289E-16,1.,0.));
#30612=DIRECTION('',(0.,0.,-1.));
#30613=DIRECTION('center_axis',(0.,-1.,0.));
#30614=DIRECTION('ref_axis',(0.,0.,-1.));
#30615=DIRECTION('',(-1.,0.,0.));
#30616=DIRECTION('',(0.,0.,-1.));
#30617=DIRECTION('',(-1.,0.,0.));
#30618=DIRECTION('center_axis',(1.,1.85037170770859E-16,0.));
#30619=DIRECTION('ref_axis',(-1.85037170770859E-16,1.,0.));
#30620=DIRECTION('',(1.85037170770859E-16,-1.,0.));
#30621=DIRECTION('',(0.,0.,-1.));
#30622=DIRECTION('',(1.85037170770859E-16,-1.,0.));
#30623=DIRECTION('center_axis',(0.,1.,0.));
#30624=DIRECTION('ref_axis',(0.,0.,1.));
#30625=DIRECTION('',(1.,0.,0.));
#30626=DIRECTION('',(1.,0.,0.));
#30627=DIRECTION('center_axis',(0.,0.,1.));
#30628=DIRECTION('ref_axis',(1.,0.,0.));
#30629=DIRECTION('center_axis',(0.,0.,1.));
#30630=DIRECTION('ref_axis',(1.,0.,0.));
#52924=CARTESIAN_POINT('',(0.,0.,0.));
#52925=CARTESIAN_POINT('Origin',(34.,25.,2.5));
#52926=CARTESIAN_POINT('',(30.7,25.,-2.5));
#52927=CARTESIAN_POINT('Origin',(34.,25.,-2.5));
#52928=CARTESIAN_POINT('',(30.7,25.,2.5));
#52929=CARTESIAN_POINT('',(30.7,25.,2.5));
#52930=CARTESIAN_POINT('Origin',(34.,25.,2.5));
#52931=CARTESIAN_POINT('Origin',(-34.,25.,2.5));
#52932=CARTESIAN_POINT('',(-37.3,25.,-2.5));
#52933=CARTESIAN_POINT('Origin',(-34.,25.,-2.5));
#52934=CARTESIAN_POINT('',(-37.3,25.,2.5));
#52935=CARTESIAN_POINT('',(-37.3,25.,2.5));
#52936=CARTESIAN_POINT('Origin',(-34.,25.,2.5));
#52937=CARTESIAN_POINT('Origin',(-34.,-25.,2.5));
#52938=CARTESIAN_POINT('',(-37.3,-25.,-2.5));
#52939=CARTESIAN_POINT('Origin',(-34.,-25.,-2.5));
#52940=CARTESIAN_POINT('',(-37.3,-25.,2.5));
#52941=CARTESIAN_POINT('',(-37.3,-25.,2.5));
#52942=CARTESIAN_POINT('Origin',(-34.,-25.,2.5));
#52943=CARTESIAN_POINT('Origin',(34.,-25.,2.5));
#52944=CARTESIAN_POINT('',(30.7,-25.,-2.5));
#52945=CARTESIAN_POINT('Origin',(34.,-25.,-2.5));
#52946=CARTESIAN_POINT('',(30.7,-25.,2.5));
#52947=CARTESIAN_POINT('',(30.7,-25.,2.5));
#52948=CARTESIAN_POINT('Origin',(34.,-25.,2.5));
#52949=CARTESIAN_POINT('Origin',(-14.,25.,2.5));
#52950=CARTESIAN_POINT('',(-17.3,25.,-2.5));
#52951=CARTESIAN_POINT('Origin',(-14.,25.,-2.5));
#52952=CARTESIAN_POINT('',(-17.3,25.,2.5));
#52953=CARTESIAN_POINT('',(-17.3,25.,2.5));
#52954=CARTESIAN_POINT('Origin',(-14.,25.,2.5));
#52955=CARTESIAN_POINT('Origin',(14.,-25.,2.5));
#52956=CARTESIAN_POINT('',(10.7,-25.,-2.5));
#52957=CARTESIAN_POINT('Origin',(14.,-25.,-2.5));
#52958=CARTESIAN_POINT('',(10.7,-25.,2.5));
#52959=CARTESIAN_POINT('',(10.7,-25.,2.5));
#52960=CARTESIAN_POINT('Origin',(14.,-25.,2.5));
#52961=CARTESIAN_POINT('Origin',(47.5,37.5,2.5));
#52962=CARTESIAN_POINT('',(47.5,-37.5,-2.5));
#52963=CARTESIAN_POINT('',(47.5,37.5,-2.5));
#52964=CARTESIAN_POINT('',(47.5,37.5,-2.5));
#52965=CARTESIAN_POINT('',(47.5,37.5,2.5));
#52966=CARTESIAN_POINT('',(47.5,37.5,2.5));
#52967=CARTESIAN_POINT('',(47.5,-37.5,2.5));
#52968=CARTESIAN_POINT('',(47.5,37.5,2.5));
#52969=CARTESIAN_POINT('',(47.5,-37.5,2.5));
#52970=CARTESIAN_POINT('Origin',(-47.5,37.5,2.5));
#52971=CARTESIAN_POINT('',(-47.5,37.5,-2.5));
#52972=CARTESIAN_POINT('',(-47.5,37.5,-2.5));
#52973=CARTESIAN_POINT('',(-47.5,37.5,2.5));
#52974=CARTESIAN_POINT('',(-47.5,37.5,2.5));
#52975=CARTESIAN_POINT('',(-47.5,37.5,2.5));
#52976=CARTESIAN_POINT('Origin',(-47.5,37.5,2.5));
#52977=CARTESIAN_POINT('',(-47.5,-37.5,-2.5));
#52978=CARTESIAN_POINT('',(-47.5,37.5,-2.5));
#52979=CARTESIAN_POINT('',(-47.5,-37.5,2.5));
#52980=CARTESIAN_POINT('',(-47.5,-37.5,2.5));
#52981=CARTESIAN_POINT('',(-47.5,37.5,2.5));
#52982=CARTESIAN_POINT('Origin',(-47.5,-37.5,2.5));
#52983=CARTESIAN_POINT('',(-47.5,-37.5,-2.5));
#52984=CARTESIAN_POINT('',(-47.5,-37.5,2.5));
#52985=CARTESIAN_POINT('Origin',(0.,0.,2.5));
#52986=CARTESIAN_POINT('Origin',(0.,0.,-2.5));
#57028=UNCERTAINTY_MEASURE_WITH_UNIT(LENGTH_MEASURE(0.01),#57080,
'DISTANCE_ACCURACY_VALUE',
'Maximum model space distance between geometric entities at asserted c
onnectivities');
#57040=UNCERTAINTY_MEASURE_WITH_UNIT(LENGTH_MEASURE(0.01),#57080,
'DISTANCE_ACCURACY_VALUE',
'Maximum model space distance between geometric entities at asserted c
onnectivities');
#57067=(
GEOMETRIC_REPRESENTATION_CONTEXT(3)
GLOBAL_UNCERTAINTY_ASSIGNED_CONTEXT((#57028))
GLOBAL_UNIT_ASSIGNED_CONTEXT((#57080,#57082,#57083))
REPRESENTATION_CONTEXT('','3D')
);
#57079=(
GEOMETRIC_REPRESENTATION_CONTEXT(3)
GLOBAL_UNCERTAINTY_ASSIGNED_CONTEXT((#57040))
GLOBAL_UNIT_ASSIGNED_CONTEXT((#57080,#57082,#57083))
REPRESENTATION_CONTEXT('','3D')
);
#57080=(
LENGTH_UNIT()
NAMED_UNIT(*)
SI_UNIT(.MILLI.,.METRE.)
);
#57082=(
NAMED_UNIT(*)
PLANE_ANGLE_UNIT()
SI_UNIT($,.RADIAN.)
);
#57083=(
NAMED_UNIT(*)
SI_UNIT($,.STERADIAN.)
SOLID_ANGLE_UNIT()
);
#57110=SHAPE_DEFINITION_REPRESENTATION(#57164,#57275);
#57164=PRODUCT_DEFINITION_SHAPE('',$,#57314);
#57275=SHAPE_REPRESENTATION('',(#26043),#57067);
#57287=PRODUCT_DEFINITION_CONTEXT('part definition',#57403,'design');
#57314=PRODUCT_DEFINITION('Ball Screw Support Spacer',
'Ball Screw Support Spacer',#57352,#57287);
#57352=PRODUCT_DEFINITION_FORMATION('',$,#57431);
#57403=APPLICATION_CONTEXT(
'Core Data for Automotive Mechanical Design Process');
#57404=PRODUCT_CONTEXT('part definition',#57403,'mechanical');
#57431=PRODUCT('Ball Screw Support Spacer','Ball Screw Support Spacer',
$,(#57404));
#57444=PRESENTATION_STYLE_ASSIGNMENT((#57446));
#57446=SURFACE_STYLE_USAGE(.BOTH.,#57448);
#57448=SURFACE_SIDE_STYLE('',(#57450));
#57450=SURFACE_STYLE_FILL_AREA(#57452);
#57452=FILL_AREA_STYLE('Opaque(202,209,238)',(#57454));
#57454=FILL_AREA_STYLE_COLOUR('Opaque(202,209,238)',#57456);
#57456=COLOUR_RGB('Opaque(202,209,238)',0.792156862745098,0.819607843137255,
0.933333333333333);
ENDSEC;
END-ISO-10303-21;
